ISO-10303-21;
HEADER;
/* Generated by software containing ST-Developer
 * from STEP Tools, Inc. (www.steptools.com) 
 */

FILE_DESCRIPTION(
/* description */ ('Jaw-coupled motor to shaft test stand'),
/* implementation_level */ '2;1');

FILE_NAME(
/* name */ 'Mounting reducer (2).step',
/* time_stamp */ '2026-10-27T10:46:06-07:00',
/* author */ (''),
/* organization */ (''),
/* preprocessor_version */ 'ST-DEVELOPER v20.2',
/* originating_system */ 'Autodesk Translation Framework v15.17.0.0',
/* authorisation */ '');

FILE_SCHEMA (('AUTOMOTIVE_DESIGN { 1 0 10303 214 3 1 1 }'));
ENDSEC;

DATA;
#10=MECHANICAL_DESIGN_GEOMETRIC_PRESENTATION_REPRESENTATION('',(#345),#19361);
#281=SHAPE_REPRESENTATION_RELATIONSHIP('SRR','None',#19495,#313);
#313=ADVANCED_BREP_SHAPE_REPRESENTATION('',(#378),#19331);
#345=STYLED_ITEM('',(#19739),#378);
#378=MANIFOLD_SOLID_BREP('Body1',#10989);
#419=FACE_BOUND('',#1693,.T.);
#420=FACE_BOUND('',#1695,.T.);
#538=PLANE('',#11439);
#539=PLANE('',#11440);
#1054=FACE_OUTER_BOUND('',#1690,.T.);
#1055=FACE_OUTER_BOUND('',#1691,.T.);
#1056=FACE_OUTER_BOUND('',#1692,.T.);
#1057=FACE_OUTER_BOUND('',#1694,.T.);
#1690=EDGE_LOOP('',(#7478,#7479,#7480,#7481));
#1691=EDGE_LOOP('',(#7482,#7483,#7484,#7485));
#1692=EDGE_LOOP('',(#7486));
#1693=EDGE_LOOP('',(#7487));
#1694=EDGE_LOOP('',(#7488));
#1695=EDGE_LOOP('',(#7489));
#2421=LINE('',#15581,#3574);
#2422=LINE('',#15587,#3575);
#3574=VECTOR('',#12510,0.425);
#3575=VECTOR('',#12517,0.645);
#4701=CIRCLE('',#11434,0.425);
#4702=CIRCLE('',#11435,0.425);
#4703=CIRCLE('',#11437,0.645);
#4704=CIRCLE('',#11438,0.645);
#4987=VERTEX_POINT('',#15578);
#4988=VERTEX_POINT('',#15580);
#4989=VERTEX_POINT('',#15584);
#4990=VERTEX_POINT('',#15586);
#5950=EDGE_CURVE('',#4987,#4987,#4701,.T.);
#5951=EDGE_CURVE('',#4987,#4988,#2421,.T.);
#5952=EDGE_CURVE('',#4988,#4988,#4702,.T.);
#5953=EDGE_CURVE('',#4989,#4989,#4703,.T.);
#5954=EDGE_CURVE('',#4989,#4990,#2422,.T.);
#5955=EDGE_CURVE('',#4990,#4990,#4704,.T.);
#7478=ORIENTED_EDGE('',*,*,#5950,.F.);
#7479=ORIENTED_EDGE('',*,*,#5951,.T.);
#7480=ORIENTED_EDGE('',*,*,#5952,.T.);
#7481=ORIENTED_EDGE('',*,*,#5951,.F.);
#7482=ORIENTED_EDGE('',*,*,#5953,.F.);
#7483=ORIENTED_EDGE('',*,*,#5954,.T.);
#7484=ORIENTED_EDGE('',*,*,#5955,.T.);
#7485=ORIENTED_EDGE('',*,*,#5954,.F.);
#7486=ORIENTED_EDGE('',*,*,#5953,.T.);
#7487=ORIENTED_EDGE('',*,*,#5950,.T.);
#7488=ORIENTED_EDGE('',*,*,#5955,.F.);
#7489=ORIENTED_EDGE('',*,*,#5952,.F.);
#10280=CYLINDRICAL_SURFACE('',#11433,0.425);
#10281=CYLINDRICAL_SURFACE('',#11436,0.645);
#10396=ADVANCED_FACE('',(#1054),#10280,.F.);
#10397=ADVANCED_FACE('',(#1055),#10281,.T.);
#10398=ADVANCED_FACE('',(#1056,#419),#538,.T.);
#10399=ADVANCED_FACE('',(#1057,#420),#539,.F.);
#10989=CLOSED_SHELL('',(#10396,#10397,#10398,#10399));
#11432=AXIS2_PLACEMENT_3D('',#15576,#12504,#12505);
#11433=AXIS2_PLACEMENT_3D('',#15577,#12506,#12507);
#11434=AXIS2_PLACEMENT_3D('',#15579,#12508,#12509);
#11435=AXIS2_PLACEMENT_3D('',#15582,#12511,#12512);
#11436=AXIS2_PLACEMENT_3D('',#15583,#12513,#12514);
#11437=AXIS2_PLACEMENT_3D('',#15585,#12515,#12516);
#11438=AXIS2_PLACEMENT_3D('',#15588,#12518,#12519);
#11439=AXIS2_PLACEMENT_3D('',#15589,#12520,#12521);
#11440=AXIS2_PLACEMENT_3D('',#15590,#12522,#12523);
#12504=DIRECTION('axis',(0.,0.,1.));
#12505=DIRECTION('refdir',(1.,0.,0.));
#12506=DIRECTION('center_axis',(0.,0.,1.));
#12507=DIRECTION('ref_axis',(1.,0.,0.));
#12508=DIRECTION('center_axis',(0.,0.,-1.));
#12509=DIRECTION('ref_axis',(1.,0.,0.));
#12510=DIRECTION('',(0.,0.,-1.));
#12511=DIRECTION('center_axis',(0.,0.,-1.));
#12512=DIRECTION('ref_axis',(1.,0.,0.));
#12513=DIRECTION('center_axis',(0.,0.,1.));
#12514=DIRECTION('ref_axis',(1.,0.,0.));
#12515=DIRECTION('center_axis',(0.,0.,1.));
#12516=DIRECTION('ref_axis',(1.,0.,0.));
#12517=DIRECTION('',(0.,0.,-1.));
#12518=DIRECTION('center_axis',(0.,0.,1.));
#12519=DIRECTION('ref_axis',(1.,0.,0.));
#12520=DIRECTION('center_axis',(0.,0.,1.));
#12521=DIRECTION('ref_axis',(1.,0.,0.));
#12522=DIRECTION('center_axis',(0.,0.,1.));
#12523=DIRECTION('ref_axis',(1.,0.,0.));
#15576=CARTESIAN_POINT('',(0.,0.,0.));
#15577=CARTESIAN_POINT('Origin',(-4.75,18.,1.2));
#15578=CARTESIAN_POINT('',(-5.175,18.,2.4));
#15579=CARTESIAN_POINT('Origin',(-4.75,18.,2.4));
#15580=CARTESIAN_POINT('',(-5.175,18.,1.2));
#15581=CARTESIAN_POINT('',(-5.175,18.,1.2));
#15582=CARTESIAN_POINT('Origin',(-4.75,18.,1.2));
#15583=CARTESIAN_POINT('Origin',(-4.75,18.,1.2));
#15584=CARTESIAN_POINT('',(-5.395,18.,2.4));
#15585=CARTESIAN_POINT('Origin',(-4.75,18.,2.4));
#15586=CARTESIAN_POINT('',(-5.395,18.,1.2));
#15587=CARTESIAN_POINT('',(-5.395,18.,1.2));
#15588=CARTESIAN_POINT('Origin',(-4.75,18.,1.2));
#15589=CARTESIAN_POINT('Origin',(-4.75,18.,2.4));
#15590=CARTESIAN_POINT('Origin',(-4.75,18.,1.2));
#19293=UNCERTAINTY_MEASURE_WITH_UNIT(LENGTH_MEASURE(0.001),#19362,
'DISTANCE_ACCURACY_VALUE',
'Maximum model space distance between geometric entities at asserted c
onnectivities');
#19323=UNCERTAINTY_MEASURE_WITH_UNIT(LENGTH_MEASURE(0.001),#19362,
'DISTANCE_ACCURACY_VALUE',
'Maximum model space distance between geometric entities at asserted c
onnectivities');
#19331=(
GEOMETRIC_REPRESENTATION_CONTEXT(3)
GLOBAL_UNCERTAINTY_ASSIGNED_CONTEXT((#19293))
GLOBAL_UNIT_ASSIGNED_CONTEXT((#19362,#19364,#19365))
REPRESENTATION_CONTEXT('','3D')
);
#19361=(
GEOMETRIC_REPRESENTATION_CONTEXT(3)
GLOBAL_UNCERTAINTY_ASSIGNED_CONTEXT((#19323))
GLOBAL_UNIT_ASSIGNED_CONTEXT((#19362,#19364,#19365))
REPRESENTATION_CONTEXT('','3D')
);
#19362=(
LENGTH_UNIT()
NAMED_UNIT(*)
SI_UNIT(.CENTI.,.METRE.)
);
#19364=(
NAMED_UNIT(*)
PLANE_ANGLE_UNIT()
SI_UNIT($,.RADIAN.)
);
#19365=(
NAMED_UNIT(*)
SI_UNIT($,.STERADIAN.)
SOLID_ANGLE_UNIT()
);
#19373=SHAPE_DEFINITION_REPRESENTATION(#19410,#19495);
#19410=PRODUCT_DEFINITION_SHAPE('',$,#19533);
#19495=SHAPE_REPRESENTATION('',(#11432),#19331);
#19525=PRODUCT_DEFINITION_CONTEXT('part definition',#19638,'design');
#19533=PRODUCT_DEFINITION('Mounting reducer (2)','Mounting reducer (2)',#19570,
#19525);
#19570=PRODUCT_DEFINITION_FORMATION('',$,#19647);
#19638=APPLICATION_CONTEXT(
'Core Data for Automotive Mechanical Design Process');
#19639=PRODUCT_CONTEXT('part definition',#19638,'mechanical');
#19647=PRODUCT('Mounting reducer (2)','Mounting reducer (2)',
'Mounting reducer (2)',(#19639));
#19733=COLOUR_RGB('Sky Blue',0.24,0.69,0.87);
#19734=FILL_AREA_STYLE_COLOUR('',#19733);
#19735=FILL_AREA_STYLE('',(#19734));
#19736=SURFACE_STYLE_FILL_AREA(#19735);
#19737=SURFACE_SIDE_STYLE('',(#19736));
#19738=SURFACE_STYLE_USAGE(.BOTH.,#19737);
#19739=PRESENTATION_STYLE_ASSIGNMENT((#19738));
ENDSEC;
END-ISO-10303-21;
